ISO-10303-21;
HEADER;
FILE_DESCRIPTION (('STEP AP203'),
    '1' );
FILE_NAME ('1602p_c_07.step',
    '2026-10-31T14:11:27',
    ( '' ),
    ( '' ),
    'SwSTEP 2.0',
    'SolidWorks 2024',
    '' );
FILE_SCHEMA (( 'AUTOMOTIVE_DESIGN' ));
ENDSEC;

DATA;
#192=EDGE_CURVE ( 'NONE', #3524, #19301, #10707, .T. ) ;
#221=DIRECTION ( 'NONE',  ( 0.9999862922474493931, 0.005235963827101436548, -1.187304881134279227E-16 ) ) ;
#230=DIRECTION ( 'NONE',  ( 1.187319687680494078E-16, 2.805478249478345354E-20, 1.000000000000000000 ) ) ;
#369=EDGE_CURVE ( 'NONE', #21866, #19301, #12226, .T. ) ;
#413=EDGE_CURVE ( 'NONE', #11749, #5148, #5943, .T. ) ;
#415=DIRECTION ( 'NONE',  ( 1.000000000000000000, 0.000000000000000000, 0.000000000000000000 ) ) ;
#447=DIRECTION ( 'NONE',  ( -0.7070970883417647679, -0.003702385528188428636, -0.7071067811865467956 ) ) ;
#527=CARTESIAN_POINT ( 'NONE',  ( -2.966462739374829791E-16, -7.772954297906289827E-16, -2.500000000000090150 ) ) ;
#541=CARTESIAN_POINT ( 'NONE',  ( -70.63306599754589854, 6.130251853413639651, -3.000000000000079936 ) ) ;
#552=FACE_OUTER_BOUND ( 'NONE', #15319, .T. ) ;
#554=VERTEX_POINT ( 'NONE', #18139 ) ;
#592=DIRECTION ( 'NONE',  ( -0.005235963827121941846, 0.9999862922474492821, 5.936218956657112052E-19 ) ) ;
#594=CARTESIAN_POINT ( 'NONE',  ( -66.29618031796869104, -0.3471291603817610039, -3.000000000000079936 ) ) ;
#629=AXIS2_PLACEMENT_3D ( 'NONE', #2608, #14751, #21978 ) ;
#697=ORIENTED_EDGE ( 'NONE', *, *, #6201, .T. ) ;
#753=CARTESIAN_POINT ( 'NONE',  ( -16.00004797695772751, -0.08377682083104273647, -8.699586588110780178E-14 ) ) ;
#774=DIRECTION ( 'NONE',  ( 4.847794496894149712E-12, 0.000000000000000000, 1.000000000000000000 ) ) ;
#802=ORIENTED_EDGE ( 'NONE', *, *, #16504, .F. ) ;
#903=VERTEX_POINT ( 'NONE', #10178 ) ;
#910=ORIENTED_EDGE ( 'NONE', *, *, #17387, .F. ) ;
#920=CARTESIAN_POINT ( 'NONE',  ( -26.68810977484059777, -6.639828994528089723, -2.501000000000090484 ) ) ;
#949=ADVANCED_FACE ( 'NONE', ( #6248 ), #2674, .F. ) ;
#951=DIRECTION ( 'NONE',  ( 0.000000000000000000, -6.936119456125000933E-16, 1.000000000000000000 ) ) ;
#971=LINE ( 'NONE', #4195, #1255 ) ;
#1027=DIRECTION ( 'NONE',  ( 0.000000000000000000, -2.739767185169287006E-14, 1.000000000000000000 ) ) ;
#1029=CIRCLE ( 'NONE', #16222, 6.499999999999997335 ) ;
#1089=DIRECTION ( 'NONE',  ( -0.005235963827121941846, 0.9999862922474492821, 5.936218956651588485E-19 ) ) ;
#1111=CIRCLE ( 'NONE', #12874, 0.0009999999999975306419 ) ;
#1232=CARTESIAN_POINT ( 'NONE',  ( -30.72441677844230057, -6.660963241697680282, -3.000000000000079936 ) ) ;
#1244=CYLINDRICAL_SURFACE ( 'NONE', #5248, 2.500999999999959922 ) ;
#1255=VECTOR ( 'NONE', #4328, 1000.000000000000000 ) ;
#1263=DIRECTION ( 'NONE',  ( 3.268868123706374574E-19, -6.243021194963094727E-17, -1.000000000000000000 ) ) ;
#1282=EDGE_CURVE ( 'NONE', #22720, #13515, #20111, .T. ) ;
#1355=EDGE_CURVE ( 'NONE', #2977, #17755, #17491, .T. ) ;
#1357=FACE_OUTER_BOUND ( 'NONE', #5510, .T. ) ;
#1371=LINE ( 'NONE', #5181, #7305 ) ;
#1387=DIRECTION ( 'NONE',  ( 0.005235963827121942714, -0.9999862922474493931, -2.738609489598291197E-14 ) ) ;
#1401=ORIENTED_EDGE ( 'NONE', *, *, #7316, .F. ) ;
#1436=DIRECTION ( 'NONE',  ( -0.9999862922474492821, -0.005235963827121953122, 1.187304881134294758E-16 ) ) ;
#1541=DIRECTION ( 'NONE',  ( -0.9999862922474492821, -0.005235963827121953122, 1.187304881134294758E-16 ) ) ;
#1638=CIRCLE ( 'NONE', #3163, 3.499999999999998668 ) ;
#1748=CARTESIAN_POINT ( 'NONE',  ( 0.03403376487640559500, -6.499910899608420500, -2.500000000000090150 ) ) ;
#1762=CARTESIAN_POINT ( 'NONE',  ( -26.75688440168130100, 6.359989102302520791, -2.500292893218799772 ) ) ;
#1777=EDGE_LOOP ( 'NONE', ( #15987, #12154, #3454, #18818, #13999, #11383, #9608, #3929, #11992, #18480, #4171, #13920 ) ) ;
#1779=EDGE_CURVE ( 'NONE', #22384, #22303, #6078, .T. ) ;
#1795=EDGE_CURVE ( 'NONE', #7126, #13085, #21247, .T. ) ;
#1834=CIRCLE ( 'NONE', #20814, 2.500999999999919954 ) ;
#1892=DIRECTION ( 'NONE',  ( -0.9999862922474492821, -0.005235963827121953122, 1.187304881134294758E-16 ) ) ;
#1914=ORIENTED_EDGE ( 'NONE', *, *, #1282, .T. ) ;
#2108=EDGE_CURVE ( 'NONE', #21983, #22720, #10113, .T. ) ;
#2116=AXIS2_PLACEMENT_3D ( 'NONE', #22136, #20361, #22595 ) ;
#2117=DIRECTION ( 'NONE',  ( 0.005235963827104182615, -0.9999862922474495042, -5.936218956636744380E-19 ) ) ;
#2138=ORIENTED_EDGE ( 'NONE', *, *, #1795, .T. ) ;
#2203=CARTESIAN_POINT ( 'NONE',  ( -28.95596696049959817, -6.651703575491109355, -4.767474059747899950 ) ) ;
#2232=AXIS2_PLACEMENT_3D ( 'NONE', #15132, #22370, #6116 ) ;
#2258=EDGE_CURVE ( 'NONE', #17265, #18737, #5331, .T. ) ;
#2262=( NAMED_UNIT ( * ) PLANE_ANGLE_UNIT ( ) SI_UNIT ( $, .RADIAN. ) );
#2282=ORIENTED_EDGE ( 'NONE', *, *, #13473, .T. ) ;
#2331=APPLICATION_CONTEXT ( 'configuration controlled 3d designs of mechanical parts and assemblies' ) ;
#2366=ORIENTED_EDGE ( 'NONE', *, *, #4147, .T. ) ;
#2459=DIRECTION ( 'NONE',  ( -0.9999862922474492821, -0.005235963827121951387, 1.187304881134294758E-16 ) ) ;
#2477=EDGE_LOOP ( 'NONE', ( #22469, #21912, #14878, #15493 ) ) ;
#2481=VECTOR ( 'NONE', #17324, 1000.000000000000114 ) ;
#2493=DIRECTION ( 'NONE',  ( -0.9999862922474492821, -0.005235963827121953122, 1.239088197126291310E-16 ) ) ;
#2507=ADVANCED_FACE ( 'NONE', ( #13478, #7779, #20711 ), #11607, .F. ) ;
#2569=CARTESIAN_POINT ( 'NONE',  ( 0.000000000000000000, 0.000000000000000000, 0.000000000000000000 ) ) ;
#2583=PLANE ( 'NONE',  #9142 ) ;
#2608=CARTESIAN_POINT ( 'NONE',  ( -26.68881687192900287, -6.639832696913689603, -2.500292893218899692 ) ) ;
#2626=SHAPE_REPRESENTATION_RELATIONSHIP ( 'NONE' , 'NONE' ,  #21569, #3149 ) ;
#2636=CARTESIAN_POINT ( 'NONE',  ( -2.966462739374829791E-16, -7.772954297906289827E-16, -2.500000000000090150 ) ) ;
#2674=CYLINDRICAL_SURFACE ( 'NONE', #7218, 3.499999999999998668 ) ;
#2776=CARTESIAN_POINT ( 'NONE',  ( -26.68881687192900287, -6.639832696913689603, -2.500292893218899692 ) ) ;
#2907=CARTESIAN_POINT ( 'NONE',  ( 0.03403376487640590031, -6.499910899608420500, -8.889944397045749129E-14 ) ) ;
#2930=FACE_BOUND ( 'NONE', #3287, .T. ) ;
#2940=DIRECTION ( 'NONE',  ( -0.9999862922474492821, -0.005235963827122071951, 1.187304881134280213E-16 ) ) ;
#2977=VERTEX_POINT ( 'NONE', #8303 ) ;
#2982=CARTESIAN_POINT ( 'NONE',  ( -69.90454993788389970, 6.134066389561166233, -3.000000000000079936 ) ) ;
#3023=DIRECTION ( 'NONE',  ( -0.9999862922474492821, -0.005235963827121951387, 1.187304881134294758E-16 ) ) ;
#3054=ADVANCED_FACE ( 'NONE', ( #7520 ), #15313, .T. ) ;
#3080=VECTOR ( 'NONE', #20475, 1000.000000000000114 ) ;
#3110=EDGE_LOOP ( 'NONE', ( #6015, #12221, #8373, #9509 ) ) ;
#3120=AXIS2_PLACEMENT_3D ( 'NONE', #5126, #12381, #17830 ) ;
#3149=ADVANCED_BREP_SHAPE_REPRESENTATION ( '', ( #9741, #12739 ), #21969 ) ;
#3163=AXIS2_PLACEMENT_3D ( 'NONE', #527, #18477, #15127 ) ;
#3185=CIRCLE ( 'NONE', #6222, 6.499999999999997335 ) ;
#3214=PRODUCT_DEFINITION_SHAPE ( 'NONE', 'NONE',  #8957 ) ;
#3239=ORIENTED_EDGE ( 'NONE', *, *, #369, .F. ) ;
#3240=DIRECTION ( 'NONE',  ( 0.005235963827102643048, -0.9999862922474495042, -7.724582913192744961E-15 ) ) ;
#3281=CARTESIAN_POINT ( 'NONE',  ( -69.90454993788326021, 6.134066389438223688, 0.7502499999999270308 ) ) ;
#3287=EDGE_LOOP ( 'NONE', ( #3604, #18327 ) ) ;
#3314=VERTEX_POINT ( 'NONE', #7229 ) ;
#3335=CARTESIAN_POINT ( 'NONE',  ( -19.49999999982379961, -0.1021026942259700004, -8.658030917271079259E-14 ) ) ;
#3338=ORIENTED_EDGE ( 'NONE', *, *, #17575, .T. ) ;
#3344=DIRECTION ( 'NONE',  ( 0.000000000000000000, 0.000000000000000000, 1.000000000000000000 ) ) ;
#3432=DIRECTION ( 'NONE',  ( 0.000000000000000000, -6.936119456124777094E-16, 1.000000000000000000 ) ) ;
#3454=ORIENTED_EDGE ( 'NONE', *, *, #1795, .F. ) ;
#3485=EDGE_CURVE ( 'NONE', #21440, #13431, #5728, .T. ) ;
#3507=CARTESIAN_POINT ( 'NONE',  ( -0.03403376487617940094, 6.499910899608420500, -8.889172688581379631E-14 ) ) ;
#3524=VERTEX_POINT ( 'NONE', #19098 ) ;
#3540=ADVANCED_FACE ( 'NONE', ( #18758 ), #2583, .F. ) ;
#3604=ORIENTED_EDGE ( 'NONE', *, *, #23415, .T. ) ;
#3613=CIRCLE ( 'NONE', #8563, 2.501000000000000334 ) ;
#3623=DIRECTION ( 'NONE',  ( -1.187319687680499994E-16, -2.805478249478640262E-20, -1.000000000000000000 ) ) ;
#3654=ADVANCED_FACE ( 'NONE', ( #8880, #2930, #6853 ), #19435, .T. ) ;
#3680=DIRECTION ( 'NONE',  ( -1.187319687680494078E-16, -2.805478249478345354E-20, -1.000000000000000000 ) ) ;
#3715=ORIENTED_EDGE ( 'NONE', *, *, #7639, .F. ) ;
#3718=AXIS2_PLACEMENT_3D ( 'NONE', #13774, #13883, #10105 ) ;
#3769=LINE ( 'NONE', #11047, #18317 ) ;
#3912=DIRECTION ( 'NONE',  ( 0.005235963827121942714, -0.9999862922474493931, -2.738609489598291197E-14 ) ) ;
#3929=ORIENTED_EDGE ( 'NONE', *, *, #413, .T. ) ;
#4026=DIRECTION ( 'NONE',  ( 0.000000000000000000, -2.710505431696529444E-14, 1.000000000000000000 ) ) ;
#4048=FACE_OUTER_BOUND ( 'NONE', #10203, .T. ) ;
#4051=DIRECTION ( 'NONE',  ( 0.000000000000000000, -2.739767185169682068E-14, 1.000000000000000000 ) ) ;
#4064=CARTESIAN_POINT ( 'NONE',  ( -30.75845054331819739, -0.1610523420890279944, -2.999000000000079602 ) ) ;
#4071=ORIENTED_EDGE ( 'NONE', *, *, #12962, .T. ) ;
#4085=DIRECTION ( 'NONE',  ( 0.005235963827121941846, -0.9999862922474492821, -5.936218956657112052E-19 ) ) ;
#4093=CARTESIAN_POINT ( 'NONE',  ( -60.06514239919540188, -6.814592325618320068, -5.500000000000079048 ) ) ;
#4094=AXIS2_PLACEMENT_3D ( 'NONE', #9594, #11626, #2459 ) ;
#4147=EDGE_CURVE ( 'NONE', #20385, #3524, #19408, .T. ) ;
#4171=ORIENTED_EDGE ( 'NONE', *, *, #13106, .T. ) ;
#4182=DIRECTION ( 'NONE',  ( -0.9999862922474492821, -0.005235963827121951387, 1.239088197126291310E-16 ) ) ;
#4195=CARTESIAN_POINT ( 'NONE',  ( -3.499952022866071211, -0.01832587339492760051, -8.848002871973867878E-14 ) ) ;
#4235=CARTESIAN_POINT ( 'NONE',  ( -30.79248430819469817, 6.338858557518999959, -5.500000000000089706 ) ) ;
#4252=EDGE_LOOP ( 'NONE', ( #17084, #10538, #21689, #10347 ) ) ;
#4283=CIRCLE ( 'NONE', #3120, 0.0009999999996440807337 ) ;
#4305=DIRECTION ( 'NONE',  ( -1.187319687680494078E-16, -2.805478249478340539E-20, -1.000000000000000000 ) ) ;
#4328=DIRECTION ( 'NONE',  ( -1.187319687680494078E-16, -2.805478249478340539E-20, -1.000000000000000000 ) ) ;
#4329=VECTOR ( 'NONE', #1263, 1000.000000000000000 ) ;
#4347=ORIENTED_EDGE ( 'NONE', *, *, #13493, .F. ) ;
#4349=FACE_OUTER_BOUND ( 'NONE', #21255, .T. ) ;
#4362=CARTESIAN_POINT ( 'NONE',  ( -3.499952022866071211, -0.01832587339492760051, -8.848002871973867878E-14 ) ) ;
#4368=VECTOR ( 'NONE', #17558, 1000.000000000000000 ) ;
#4392=AXIS2_PLACEMENT_3D ( 'NONE', #8895, #23463, #12794 ) ;
#4412=ORIENTED_EDGE ( 'NONE', *, *, #23193, .F. ) ;
#4542=DIRECTION ( 'NONE',  ( -0.005235963827102643048, 0.9999862922474495042, 7.724582913192744961E-15 ) ) ;
#4581=LINE ( 'NONE', #19539, #10384 ) ;
#4883=VECTOR ( 'NONE', #5904, 1000.000000000000114 ) ;
#4976=LINE ( 'NONE', #18890, #11134 ) ;
#5046=CARTESIAN_POINT ( 'NONE',  ( -26.68810977484059777, -6.639828994528159889, -2.500000000000090150 ) ) ;
#5068=AXIS2_PLACEMENT_3D ( 'NONE', #13683, #19041, #1436 ) ;
#5081=ORIENTED_EDGE ( 'NONE', *, *, #18496, .F. ) ;
#5126=CARTESIAN_POINT ( 'NONE',  ( -26.75617730459320143, 6.359992804688050505, -2.500999999999729884 ) ) ;
#5148=VERTEX_POINT ( 'NONE', #13534 ) ;
#5181=CARTESIAN_POINT ( 'NONE',  ( -70.63306599754589854, 6.130251853413639651, -5.500000000000079048 ) ) ;
#5248=AXIS2_PLACEMENT_3D ( 'NONE', #8622, #6841, #6618 ) ;
#5251=LINE ( 'NONE', #21408, #18540 ) ;
#5331=LINE ( 'NONE', #7472, #19942 ) ;
#5510=EDGE_LOOP ( 'NONE', ( #1914, #21959, #4347, #22692 ) ) ;
#5528=ORIENTED_EDGE ( 'NONE', *, *, #16814, .T. ) ;
#5613=ADVANCED_FACE ( 'NONE', ( #4349 ), #6244, .T. ) ;
#5640=EDGE_LOOP ( 'NONE', ( #21371, #19934, #22682, #17696 ) ) ;
#5645=EDGE_CURVE ( 'NONE', #9333, #18146, #6959, .T. ) ;
#5646=ORIENTED_EDGE ( 'NONE', *, *, #16627, .F. ) ;
#5678=LINE ( 'NONE', #1762, #15669 ) ;
#5710=CARTESIAN_POINT ( 'NONE',  ( 3.499952022866071211, 0.01832587339492647641, -8.931114213653268455E-14 ) ) ;
#5728=CIRCLE ( 'NONE', #21277, 3.499999999999998668 ) ;
#5784=AXIS2_PLACEMENT_3D ( 'NONE', #14150, #3680, #1892 ) ;
#5834=ORIENTED_EDGE ( 'NONE', *, *, #21176, .T. ) ;
#5840=DIRECTION ( 'NONE',  ( 3.330999558957018649E-36, 2.805478249471640109E-20, 1.000000000000000000 ) ) ;
#5844=VECTOR ( 'NONE', #7260, 999.9999999999998863 ) ;
#5853=DIRECTION ( 'NONE',  ( -0.005235963827101446956, 0.9999862922474495042, 5.492442074325198113E-16 ) ) ;
#5871=LINE ( 'NONE', #20352, #8099 ) ;
#5904=DIRECTION ( 'NONE',  ( -0.7070970883417647679, -0.003702385528188428636, -0.7071067811865467956 ) ) ;
#5908=CARTESIAN_POINT ( 'NONE',  ( 3.499952022866072543, 0.01832587339492648335, -2.500000000000090594 ) ) ;
#5943=LINE ( 'NONE', #19213, #13570 ) ;
#5945=CARTESIAN_POINT ( 'NONE',  ( -29.02403449025189985, 6.348118223725100151, -4.767474059747799586 ) ) ;
#5947=CARTESIAN_POINT ( 'NONE',  ( -30.79248430819439974, 6.338858557519069237, -2.999000000000079602 ) ) ;
#5963=FACE_OUTER_BOUND ( 'NONE', #7384, .T. ) ;
#6015=ORIENTED_EDGE ( 'NONE', *, *, #4147, .F. ) ;
#6016=DIRECTION ( 'NONE',  ( -0.005235963827102643048, 0.9999862922474495042, 7.724582913192744961E-15 ) ) ;
#6049=CARTESIAN_POINT ( 'NONE',  ( -60.06514239919540188, -6.814592325618320068, -3.000000000000079936 ) ) ;
#6078=CIRCLE ( 'NONE', #22377, 2.500999999999639734 ) ;
#6116=DIRECTION ( 'NONE',  ( -0.005235963827110361700, 0.9999862922474493931, 0.000000000000000000 ) ) ;
#6140=CARTESIAN_POINT ( 'NONE',  ( -72.77122628570259621, -6.881121833202230142, 0.01852613985923039913 ) ) ;
#6177=ORIENTED_EDGE ( 'NONE', *, *, #13473, .F. ) ;
#6201=EDGE_CURVE ( 'NONE', #554, #903, #1111, .T. ) ;
#6222=AXIS2_PLACEMENT_3D ( 'NONE', #16728, #7382, #18539 ) ;
#6244=PLANE ( 'NONE',  #2232 ) ;
#6248=FACE_OUTER_BOUND ( 'NONE', #21816, .T. ) ;
#6265=DIRECTION ( 'NONE',  ( -1.187319687680494078E-16, -2.805478249478345354E-20, -1.000000000000000000 ) ) ;
#6266=UNCERTAINTY_MEASURE_WITH_UNIT (LENGTH_MEASURE( 1.000000000000000082E-05 ), #13093, 'distance_accuracy_value', 'NONE');
#6280=ORIENTED_EDGE ( 'NONE', *, *, #1355, .T. ) ;
#6427=ORIENTED_EDGE ( 'NONE', *, *, #5645, .T. ) ;
#6438=DIRECTION ( 'NONE',  ( -0.005235963827101452160, 0.9999862922474493931, 5.492442074325202057E-16 ) ) ;
#6596=ORIENTED_EDGE ( 'NONE', *, *, #17781, .F. ) ;
#6618=DIRECTION ( 'NONE',  ( 0.000000000000000000, -5.527220191599521464E-16, 1.000000000000000000 ) ) ;
#6622=CARTESIAN_POINT ( 'NONE',  ( -28.45655959278310121, -6.649088660734180145, -0.7325259402522680263 ) ) ;
#6640=EDGE_CURVE ( 'NONE', #15872, #22384, #18900, .T. ) ;
#6670=DIRECTION ( 'NONE',  ( -0.005235963827101452160, 0.9999862922474493931, 5.492442074325202057E-16 ) ) ;
#6712=ORIENTED_EDGE ( 'NONE', *, *, #17655, .T. ) ;
#6761=ORIENTED_EDGE ( 'NONE', *, *, #5645, .F. ) ;
#6834=LINE ( 'NONE', #1232, #11138 ) ;
#6841=DIRECTION ( 'NONE',  ( -0.005235963827101446956, 0.9999862922474495042, 5.492442074325198113E-16 ) ) ;
#6852=LINE ( 'NONE', #14085, #21482 ) ;
#6853=FACE_OUTER_BOUND ( 'NONE', #4252, .T. ) ;
#6858=AXIS2_PLACEMENT_3D ( 'NONE', #5947, #11439, #13207 ) ;
#6905=PLANE ( 'NONE',  #18720 ) ;
#6959=LINE ( 'NONE', #2907, #18982 ) ;
#6971=EDGE_CURVE ( 'NONE', #3314, #20139, #3769, .T. ) ;
#7025=DIRECTION ( 'NONE',  ( -5.163058955534739404E-35, -6.243192354061819367E-17, -1.000000000000000000 ) ) ;
#7126=VERTEX_POINT ( 'NONE', #17297 ) ;
#7218=AXIS2_PLACEMENT_3D ( 'NONE', #19189, #19302, #3023 ) ;
#7229=CARTESIAN_POINT ( 'NONE',  ( -69.83648240813081998, -6.865755409778300233, -5.500000000000079048 ) ) ;
#7260=DIRECTION ( 'NONE',  ( 0.005235963827102643048, -0.9999862922474495042, -7.724582913192744961E-15 ) ) ;
#7276=CARTESIAN_POINT ( 'NONE',  ( 0.03403376487640590031, -6.499910899608420500, -8.889944397045749129E-14 ) ) ;
#7305=VECTOR ( 'NONE', #12218, 1000.000000000000000 ) ;
#7316=EDGE_CURVE ( 'NONE', #13648, #554, #4581, .T. ) ;
#7341=FACE_OUTER_BOUND ( 'NONE', #5640, .T. ) ;
#7382=DIRECTION ( 'NONE',  ( 1.187319687680499994E-16, 2.805478249478695031E-20, 1.000000000000000000 ) ) ;
#7384=EDGE_LOOP ( 'NONE', ( #9045, #22813, #18990, #2138 ) ) ;
#7472=CARTESIAN_POINT ( 'NONE',  ( -69.88753305544580030, 2.884110939634079607, -3.000000000000079936 ) ) ;
#7489=LINE ( 'NONE', #6049, #9211 ) ;
#7520=FACE_OUTER_BOUND ( 'NONE', #8001, .T. ) ;
#7600=EDGE_LOOP ( 'NONE', ( #6280, #16640, #14563, #14744 ) ) ;
#7639=EDGE_CURVE ( 'NONE', #5148, #18943, #5871, .T. ) ;
#7684=CARTESIAN_POINT ( 'NONE',  ( -26.68881687192900287, -6.639832696913689603, -2.500292893218899692 ) ) ;
#7724=LINE ( 'NONE', #22075, #5844 ) ;
#7778=ADVANCED_FACE ( 'NONE', ( #8916 ), #6905, .F. ) ;
#7779=FACE_BOUND ( 'NONE', #19444, .T. ) ;
#7826=EDGE_CURVE ( 'NONE', #17755, #21398, #5678, .T. ) ;
#7833=ADVANCED_FACE ( 'NONE', ( #12934 ), #18168, .F. ) ;
#7902=VECTOR ( 'NONE', #4305, 1000.000000000000000 ) ;
#7913=EDGE_CURVE ( 'NONE', #18943, #2977, #16419, .T. ) ;
#8001=EDGE_LOOP ( 'NONE', ( #10515, #22314, #22249, #2282 ) ) ;
#8099=VECTOR ( 'NONE', #4085, 1000.000000000000114 ) ;
#8190=FACE_OUTER_BOUND ( 'NONE', #17157, .T. ) ;
#8303=CARTESIAN_POINT ( 'NONE',  ( -26.68881687192900287, -6.639832696913689603, -2.500292893218899692 ) ) ;
#8373=ORIENTED_EDGE ( 'NONE', *, *, #369, .T. ) ;
#8563=AXIS2_PLACEMENT_3D ( 'NONE', #920, #1387, #1027 ) ;
#8622=CARTESIAN_POINT ( 'NONE',  ( -30.75845054331819739, -0.1610523420890130064, -2.999000000000079602 ) ) ;
#8880=FACE_BOUND ( 'NONE', #13533, .T. ) ;
#8886=ORIENTED_EDGE ( 'NONE', *, *, #2108, .F. ) ;
#8895=CARTESIAN_POINT ( 'NONE',  ( 1.836479826415680084E-19, -7.772252928343919938E-16, -8.889558542813568797E-14 ) ) ;
#8916=FACE_OUTER_BOUND ( 'NONE', #1777, .T. ) ;
#8957=PRODUCT_DEFINITION ( 'UNKNOWN', '', #22008, #22743 ) ;
#9020=DIRECTION ( 'NONE',  ( -0.005235963827104182615, 0.9999862922474495042, 5.936218956635594600E-19 ) ) ;
#9028=EDGE_CURVE ( 'NONE', #22900, #11749, #23441, .T. ) ;
#9037=CYLINDRICAL_SURFACE ( 'NONE', #22498, 6.499999999999997335 ) ;
#9045=ORIENTED_EDGE ( 'NONE', *, *, #20558, .F. ) ;
#9142=AXIS2_PLACEMENT_3D ( 'NONE', #6140, #13394, #774 ) ;
#9211=VECTOR ( 'NONE', #221, 1000.000000000000114 ) ;
#9234=PLANE ( 'NONE',  #14998 ) ;
#9266=DIRECTION ( 'NONE',  ( 0.005235963827121942714, -0.9999862922474493931, -2.738609489598291197E-14 ) ) ;
#9333=VERTEX_POINT ( 'NONE', #11954 ) ;
#9401=CARTESIAN_POINT ( 'NONE',  ( -19.49999999982379961, -0.1021026942259700004, -2.500000000000090150 ) ) ;
#9470=ORIENTED_EDGE ( 'NONE', *, *, #9028, .F. ) ;
#9509=ORIENTED_EDGE ( 'NONE', *, *, #192, .F. ) ;
#9519=PLANE ( 'NONE',  #11653 ) ;
#9530=LINE ( 'NONE', #5710, #7902 ) ;
#9594=CARTESIAN_POINT ( 'NONE',  ( 1.836479826415680084E-19, -7.772252928343919938E-16, -8.889558542813568797E-14 ) ) ;
#9608=ORIENTED_EDGE ( 'NONE', *, *, #9028, .T. ) ;
#9741=MANIFOLD_SOLID_BREP ( 'Cut-Extrude1', #21564 ) ;
#9874=CARTESIAN_POINT ( 'NONE',  ( -26.68810977484059777, -6.639828994528159889, -8.572666733291279949E-14 ) ) ;
#9882=( NAMED_UNIT ( * ) SI_UNIT ( $, .STERADIAN. ) SOLID_ANGLE_UNIT ( ) );
#10105=DIRECTION ( 'NONE',  ( -0.9999862922474492821, -0.005235963827121953122, 1.187304881134294758E-16 ) ) ;
#10113=CIRCLE ( 'NONE', #12743, 2.501000000000000334 ) ;
#10178=CARTESIAN_POINT ( 'NONE',  ( -30.72441677844230057, -6.660963241697680282, -3.000000000000079936 ) ) ;
#10203=EDGE_LOOP ( 'NONE', ( #13041, #19124, #10849, #22540 ) ) ;
#10341=CARTESIAN_POINT ( 'NONE',  ( -0.03403376487617969931, 6.499910899608420500, -2.500000000000090150 ) ) ;
#10347=ORIENTED_EDGE ( 'NONE', *, *, #21176, .F. ) ;
#10383=CARTESIAN_POINT ( 'NONE',  ( -30.72441677844210162, -6.660963241697129611, -2.999000000000090260 ) ) ;
#10384=VECTOR ( 'NONE', #22618, 1000.000000000000114 ) ;
#10515=ORIENTED_EDGE ( 'NONE', *, *, #13493, .T. ) ;
#10529=CARTESIAN_POINT ( 'NONE',  ( -26.75617730459320143, 6.359992804688680224, -8.571895024826909188E-14 ) ) ;
#10538=ORIENTED_EDGE ( 'NONE', *, *, #21929, .F. ) ;
#10543=DIRECTION ( 'NONE',  ( 0.9999862922474492821, 0.005235963827122071951, -1.187304881134280213E-16 ) ) ;
#10602=DIRECTION ( 'NONE',  ( -1.187319687680494078E-16, -2.805478249478345354E-20, -1.000000000000000000 ) ) ;
#10676=DIRECTION ( 'NONE',  ( 0.005235963827110373843, -0.9999862922474493931, 0.000000000000000000 ) ) ;
#10678=EDGE_CURVE ( 'NONE', #3314, #22720, #15251, .T. ) ;
#10707=CIRCLE ( 'NONE', #16746, 3.499999999999998224 ) ;
#10765=ORIENTED_EDGE ( 'NONE', *, *, #22601, .T. ) ;
#10788=ORIENTED_EDGE ( 'NONE', *, *, #7913, .F. ) ;
#10797=VECTOR ( 'NONE', #3623, 1000.000000000000000 ) ;
#10798=ORIENTED_EDGE ( 'NONE', *, *, #23202, .F. ) ;
#10849=ORIENTED_EDGE ( 'NONE', *, *, #20558, .T. ) ;
#10954=DIRECTION ( 'NONE',  ( 1.187319687680494078E-16, 2.805478249478345354E-20, 1.000000000000000000 ) ) ;
#10988=LINE ( 'NONE', #18098, #16804 ) ;
#11047=CARTESIAN_POINT ( 'NONE',  ( -69.88753305544580030, 2.884110939634079607, -5.500000000000079048 ) ) ;
#11129=AXIS2_PLACEMENT_3D ( 'NONE', #12821, #3912, #4026 ) ;
#11134=VECTOR ( 'NONE', #11773, 1000.000000000000114 ) ;
#11138=VECTOR ( 'NONE', #21073, 1000.000000000000114 ) ;
#11140=CARTESIAN_POINT ( 'NONE',  ( -69.83648240813148789, -6.865755409778319773, -3.000000000000079936 ) ) ;
#11192=CARTESIAN_POINT ( 'NONE',  ( -26.68810977484059777, -6.639828994528159889, -2.501000000000090484 ) ) ;
#11326=DIRECTION ( 'NONE',  ( 1.000000000000000000, -1.187319687680469919E-16, 5.345529420184390105E-52 ) ) ;
#11383=ORIENTED_EDGE ( 'NONE', *, *, #21929, .T. ) ;
#11439=DIRECTION ( 'NONE',  ( -0.005235963827101452160, 0.9999862922474493931, 5.492442074325202057E-16 ) ) ;
#11607=PLANE ( 'NONE',  #2116 ) ;
#11616=ORIENTED_EDGE ( 'NONE', *, *, #413, .F. ) ;
#11626=DIRECTION ( 'NONE',  ( -1.187319687680494078E-16, -2.805478249478340539E-20, -1.000000000000000000 ) ) ;
#11653=AXIS2_PLACEMENT_3D ( 'NONE', #594, #5840, #11326 ) ;
#11669=ORIENTED_EDGE ( 'NONE', *, *, #19242, .F. ) ;
#11741=ADVANCED_FACE ( 'NONE', ( #8190 ), #19130, .F. ) ;
#11749=VERTEX_POINT ( 'NONE', #10341 ) ;
#11773=DIRECTION ( 'NONE',  ( -0.7070970883417647679, -0.003702385528188428636, -0.7071067811865467956 ) ) ;
#11781=ORIENTED_EDGE ( 'NONE', *, *, #16143, .T. ) ;
#11854=ORIENTED_EDGE ( 'NONE', *, *, #23193, .T. ) ;
#11859=CYLINDRICAL_SURFACE ( 'NONE', #17724, 2.500999999999819590 ) ;
#11954=CARTESIAN_POINT ( 'NONE',  ( 0.03403376487640590031, -6.499910899608420500, -8.889944397045749129E-14 ) ) ;
#11992=ORIENTED_EDGE ( 'NONE', *, *, #16524, .T. ) ;
#12023=ADVANCED_FACE ( 'NONE', ( #13147 ), #20381, .F. ) ;
#12099=CARTESIAN_POINT ( 'NONE',  ( -22.99995202268987171, -0.1204285676208968203, -8.616475246431379602E-14 ) ) ;
#12112=CARTESIAN_POINT ( 'NONE',  ( 0.03403376487640559500, -6.499910899608420500, -2.500000000000090150 ) ) ;
#12147=DIRECTION ( 'NONE',  ( -0.005235963827121941846, 0.9999862922474492821, 5.936218956651588485E-19 ) ) ;
#12153=ADVANCED_FACE ( 'NONE', ( #1357 ), #1244, .T. ) ;
#12154=ORIENTED_EDGE ( 'NONE', *, *, #21966, .T. ) ;
#12168=CARTESIAN_POINT ( 'NONE',  ( -30.72441677844230057, -6.660963241697680282, -5.500000000000089706 ) ) ;
#12218=DIRECTION ( 'NONE',  ( -0.9999862922474493931, -0.005235963827116132258, 1.187304881134280213E-16 ) ) ;
#12221=ORIENTED_EDGE ( 'NONE', *, *, #17575, .F. ) ;
#12226=LINE ( 'NONE', #18667, #4368 ) ;
#12266=AXIS2_PLACEMENT_3D ( 'NONE', #13078, #18541, #22195 ) ;
#12381=DIRECTION ( 'NONE',  ( 0.005235963827121942714, -0.9999862922474493931, -2.738609489598291197E-14 ) ) ;
#12436=VECTOR ( 'NONE', #6016, 999.9999999999998863 ) ;
#12523=PRODUCT ( '1602p_c_07', '1602p_c_07', '', ( #12837 ) ) ;
#12639=VECTOR ( 'NONE', #19181, 1000.000000000000000 ) ;
#12738=CARTESIAN_POINT ( 'NONE',  ( -26.75617730459320143, 6.359992804688110901, -2.500999999999729884 ) ) ;
#12739=AXIS2_PLACEMENT_3D ( 'NONE', #2569, #13380, #415 ) ;
#12740=EDGE_CURVE ( 'NONE', #22303, #13648, #5251, .T. ) ;
#12743=AXIS2_PLACEMENT_3D ( 'NONE', #21134, #6670, #3432 ) ;
#12794=DIRECTION ( 'NONE',  ( -0.9999862922474492821, -0.005235963827121951387, 1.187304881134294758E-16 ) ) ;
#12821=CARTESIAN_POINT ( 'NONE',  ( -26.72214353971689960, -0.1399180949200569957, -2.500999999999910184 ) ) ;
#12837=MECHANICAL_CONTEXT ( 'NONE', #15501, 'mechanical' ) ;
#12874=AXIS2_PLACEMENT_3D ( 'NONE', #10383, #6438, #3344 ) ;
#12929=CARTESIAN_POINT ( 'NONE',  ( -0.03403376487617940094, 6.499910899608420500, -8.889172688581379631E-14 ) ) ;
#12934=FACE_OUTER_BOUND ( 'NONE', #7600, .T. ) ;
#12962=EDGE_CURVE ( 'NONE', #21440, #15675, #9530, .T. ) ;
#12977=DIRECTION ( 'NONE',  ( 0.000000000000000000, 0.000000000000000000, 1.000000000000000000 ) ) ;
#12994=AXIS2_PLACEMENT_3D ( 'NONE', #4064, #5853, #12977 ) ;
#13041=ORIENTED_EDGE ( 'NONE', *, *, #2258, .T. ) ;
#13069=DIRECTION ( 'NONE',  ( 0.000000000000000000, 0.000000000000000000, 1.000000000000000000 ) ) ;
#13078=CARTESIAN_POINT ( 'NONE',  ( -66.29618031796869104, -0.3471291603817610039, -5.500000000000079048 ) ) ;
#13085=VERTEX_POINT ( 'NONE', #17358 ) ;
#13093=( LENGTH_UNIT ( ) NAMED_UNIT ( * ) SI_UNIT ( .MILLI., .METRE. ) );
#13106=EDGE_CURVE ( 'NONE', #21398, #13515, #1834, .T. ) ;
#13147=FACE_OUTER_BOUND ( 'NONE', #2477, .T. ) ;
#13154=DIRECTION ( 'NONE',  ( 0.005235963827121942714, -0.9999862922474493931, -2.738609489598291197E-14 ) ) ;
#13207=DIRECTION ( 'NONE',  ( 0.000000000000000000, 0.000000000000000000, 1.000000000000000000 ) ) ;
#13253=LINE ( 'NONE', #541, #23002 ) ;
#13380=DIRECTION ( 'NONE',  ( 0.000000000000000000, 0.000000000000000000, 1.000000000000000000 ) ) ;
#13394=DIRECTION ( 'NONE',  ( -0.005235963827063078342, 0.9999862922474496152, 2.538287662677322384E-14 ) ) ;
#13431=VERTEX_POINT ( 'NONE', #4362 ) ;
#13473=EDGE_CURVE ( 'NONE', #2977, #21983, #18857, .T. ) ;
#13478=FACE_BOUND ( 'NONE', #23332, .T. ) ;
#13493=EDGE_CURVE ( 'NONE', #21983, #21398, #15040, .T. ) ;
#13515=VERTEX_POINT ( 'NONE', #4235 ) ;
#13533=EDGE_LOOP ( 'NONE', ( #3338, #23128 ) ) ;
#13534=CARTESIAN_POINT ( 'NONE',  ( -26.75617730459320143, 6.359992804688680224, -2.500000000000090150 ) ) ;
#13570=VECTOR ( 'NONE', #2940, 1000.000000000000114 ) ;
#13648=VERTEX_POINT ( 'NONE', #6622 ) ;
#13683=CARTESIAN_POINT ( 'NONE',  ( -19.49999999982379961, -0.1021026942259700004, -8.658030917271079259E-14 ) ) ;
#13758=LINE ( 'NONE', #12112, #2481 ) ;
#13774=CARTESIAN_POINT ( 'NONE',  ( -19.49999999982379961, -0.1021026942259700004, -8.658030917271079259E-14 ) ) ;
#13883=DIRECTION ( 'NONE',  ( -1.187319687680494078E-16, -2.805478249478340539E-20, -1.000000000000000000 ) ) ;
#13920=ORIENTED_EDGE ( 'NONE', *, *, #18496, .T. ) ;
#13942=CARTESIAN_POINT ( 'NONE',  ( -26.68810977484059777, -6.639828994528159889, -8.572666733291279949E-14 ) ) ;
#13999=ORIENTED_EDGE ( 'NONE', *, *, #1779, .F. ) ;
#14085=CARTESIAN_POINT ( 'NONE',  ( -26.75617730459320143, 6.359992804688680224, -8.571895024826909188E-14 ) ) ;
#14137=AXIS2_PLACEMENT_3D ( 'NONE', #11192, #9266, #13069 ) ;
#14150=CARTESIAN_POINT ( 'NONE',  ( -19.49999999982379961, -0.1021026942259700004, -8.658030917271079259E-14 ) ) ;
#14213=LINE ( 'NONE', #3281, #4329 ) ;
#14336=DIRECTION ( 'NONE',  ( -0.9999862922474493931, -0.005235963827110373843, 0.000000000000000000 ) ) ;
#14415=CARTESIAN_POINT ( 'NONE',  ( -28.52462712253550237, 6.350733138482030249, -0.7325259402521649976 ) ) ;
#14500=ORIENTED_EDGE ( 'NONE', *, *, #6971, .T. ) ;
#14563=ORIENTED_EDGE ( 'NONE', *, *, #7639, .T. ) ;
#14568=CARTESIAN_POINT ( 'NONE',  ( -69.90454993788326021, 6.134066389438223688, -5.500000000000079048 ) ) ;
#14623=ORIENTED_EDGE ( 'NONE', *, *, #7316, .T. ) ;
#14671=ORIENTED_EDGE ( 'NONE', *, *, #20871, .F. ) ;
#14732=DIRECTION ( 'NONE',  ( -0.9999862922474492821, -0.005235963827121953122, 1.239088197126291310E-16 ) ) ;
#14744=ORIENTED_EDGE ( 'NONE', *, *, #7913, .T. ) ;
#14751=DIRECTION ( 'NONE',  ( 0.7070970883417638797, 0.003702385528197197663, -0.7071067811865479058 ) ) ;
#14764=DIRECTION ( 'NONE',  ( -0.005235963827101446089, 0.9999862922474493931, 5.936218956632777928E-19 ) ) ;
#14878=ORIENTED_EDGE ( 'NONE', *, *, #20871, .T. ) ;
#14957=ORIENTED_EDGE ( 'NONE', *, *, #12740, .T. ) ;
#14967=SHAPE_DEFINITION_REPRESENTATION ( #3214, #21569 ) ;
#14998=AXIS2_PLACEMENT_3D ( 'NONE', #16460, #14336, #10676 ) ;
#14999=CARTESIAN_POINT ( 'NONE',  ( -30.72441677844230057, -6.660963241697680282, -5.500000000000089706 ) ) ;
#15020=ORIENTED_EDGE ( 'NONE', *, *, #17387, .T. ) ;
#15040=LINE ( 'NONE', #22272, #12436 ) ;
#15104=DIRECTION ( 'NONE',  ( 1.187319687680494078E-16, 2.805478249478345354E-20, 1.000000000000000000 ) ) ;
#15127=DIRECTION ( 'NONE',  ( -0.9999862922474492821, -0.005235963827121951387, 1.239088197126291310E-16 ) ) ;
#15132=CARTESIAN_POINT ( 'NONE',  ( -28.52462712253550237, 6.350733138482030249, -0.7325259402521649976 ) ) ;
#15251=LINE ( 'NONE', #4093, #3080 ) ;
#15260=AXIS2_PLACEMENT_3D ( 'NONE', #2636, #15104, #4182 ) ;
#15313=PLANE ( 'NONE',  #629 ) ;
#15319=EDGE_LOOP ( 'NONE', ( #14957, #10798, #18442, #19211 ) ) ;
#15347=VERTEX_POINT ( 'NONE', #17332 ) ;
#15461=CYLINDRICAL_SURFACE ( 'NONE', #5068, 3.499999999999998224 ) ;
#15463=EDGE_LOOP ( 'NONE', ( #18384, #9470, #10765, #6427 ) ) ;
#15493=ORIENTED_EDGE ( 'NONE', *, *, #16143, .F. ) ;
#15501=APPLICATION_CONTEXT ( 'configuration controlled 3d designs of mechanical parts and assemblies' ) ;
#15669=VECTOR ( 'NONE', #447, 1000.000000000000114 ) ;
#15675=VERTEX_POINT ( 'NONE', #5908 ) ;
#15713=CIRCLE ( 'NONE', #16438, 3.499999999999998224 ) ;
#15872=VERTEX_POINT ( 'NONE', #13942 ) ;
#15987=ORIENTED_EDGE ( 'NONE', *, *, #18437, .F. ) ;
#16142=DIRECTION ( 'NONE',  ( 0.005235963827197880234, -0.9999862922474489491, 6.243106773925901370E-17 ) ) ;
#16143=EDGE_CURVE ( 'NONE', #15675, #15347, #22080, .T. ) ;
#16176=ADVANCED_FACE ( 'NONE', ( #5963 ), #21982, .F. ) ;
#16222=AXIS2_PLACEMENT_3D ( 'NONE', #22701, #18930, #1089 ) ;
#16419=CIRCLE ( 'NONE', #14137, 0.0009999999999996990463 ) ;
#16424=EDGE_LOOP ( 'NONE', ( #14500, #5081, #18735, #19002 ) ) ;
#16438=AXIS2_PLACEMENT_3D ( 'NONE', #19956, #10954, #2493 ) ;
#16460=CARTESIAN_POINT ( 'NONE',  ( -69.87051617300704720, -0.3658445101694126067, 0.000000000000000000 ) ) ;
#16504=EDGE_CURVE ( 'NONE', #20385, #21866, #23219, .T. ) ;
#16511=DIRECTION ( 'NONE',  ( -0.9999862922474492821, -0.005235963827121822151, 1.187304881134280213E-16 ) ) ;
#16513=CIRCLE ( 'NONE', #4392, 3.499999999999998668 ) ;
#16524=EDGE_CURVE ( 'NONE', #5148, #17755, #4283, .T. ) ;
#16580=ORIENTED_EDGE ( 'NONE', *, *, #12740, .F. ) ;
#16601=ADVANCED_FACE ( 'NONE', ( #20541 ), #22076, .F. ) ;
#16627=EDGE_CURVE ( 'NONE', #18737, #903, #7489, .T. ) ;
#16640=ORIENTED_EDGE ( 'NONE', *, *, #16524, .F. ) ;
#16728=CARTESIAN_POINT ( 'NONE',  ( 1.129445499342539821E-13, -1.843604948991550162E-16, -2.500000000000090150 ) ) ;
#16746=AXIS2_PLACEMENT_3D ( 'NONE', #9401, #230, #14732 ) ;
#16804=VECTOR ( 'NONE', #19759, 1000.000000000000000 ) ;
#16814=EDGE_CURVE ( 'NONE', #22303, #7126, #4976, .T. ) ;
#16832=CARTESIAN_POINT ( 'NONE',  ( 1.836479826415680084E-19, -7.772252928343919938E-16, -8.889558542813568797E-14 ) ) ;
#16856=CARTESIAN_POINT ( 'NONE',  ( -26.75688440168130100, 6.359989102302520791, -2.500292893218799772 ) ) ;
#17084=ORIENTED_EDGE ( 'NONE', *, *, #22601, .F. ) ;
#17157=EDGE_LOOP ( 'NONE', ( #802, #2366, #6596, #3239 ) ) ;
#17191=DIRECTION ( 'NONE',  ( 0.000000000000000000, -2.738683416504465444E-14, 1.000000000000000000 ) ) ;
#17192=DIRECTION ( 'NONE',  ( -0.9999862922474492821, -0.005235963827121951387, 1.187304881134294758E-16 ) ) ;
#17265=VERTEX_POINT ( 'NONE', #2982 ) ;
#17297=CARTESIAN_POINT ( 'NONE',  ( -30.79177721110609767, 6.338862259904598950, -2.999707106781169585 ) ) ;
#17324=DIRECTION ( 'NONE',  ( 0.9999862922474492821, 0.005235963827121822151, -1.187304881134280213E-16 ) ) ;
#17332=CARTESIAN_POINT ( 'NONE',  ( -3.499952022866071655, -0.01832587339492760051, -2.500000000000089706 ) ) ;
#17358=CARTESIAN_POINT ( 'NONE',  ( -30.79248430819469817, 6.338858557518999959, -3.000000000000079936 ) ) ;
#17387=EDGE_CURVE ( 'NONE', #15347, #15675, #1638, .T. ) ;
#17463=DIRECTION ( 'NONE',  ( -0.005235963827101452160, 0.9999862922474493931, 5.492442074325202057E-16 ) ) ;
#17477=ADVANCED_FACE ( 'NONE', ( #17957 ), #9037, .T. ) ;
#17491=LINE ( 'NONE', #2776, #23402 ) ;
#17558=DIRECTION ( 'NONE',  ( -1.187319687680494078E-16, -2.805478249478340539E-20, -1.000000000000000000 ) ) ;
#17575=EDGE_CURVE ( 'NONE', #21866, #20385, #18763, .T. ) ;
#17617=AXIS2_PLACEMENT_3D ( 'NONE', #3335, #10602, #1541 ) ;
#17625=EDGE_CURVE ( 'NONE', #18146, #11749, #3185, .T. ) ;
#17655=EDGE_CURVE ( 'NONE', #7126, #554, #7724, .T. ) ;
#17696=ORIENTED_EDGE ( 'NONE', *, *, #18437, .T. ) ;
#17724=AXIS2_PLACEMENT_3D ( 'NONE', #22626, #13154, #17191 ) ;
#17755=VERTEX_POINT ( 'NONE', #16856 ) ;
#17781=EDGE_CURVE ( 'NONE', #19301, #3524, #15713, .T. ) ;
#17830=DIRECTION ( 'NONE',  ( 0.000000000000000000, 0.000000000000000000, 1.000000000000000000 ) ) ;
#17957=FACE_OUTER_BOUND ( 'NONE', #15463, .T. ) ;
#18098=CARTESIAN_POINT ( 'NONE',  ( -69.83648240813081998, -6.865755409778439677, 0.01852613985923039913 ) ) ;
#18114=VECTOR ( 'NONE', #14764, 1000.000000000000114 ) ;
#18139=CARTESIAN_POINT ( 'NONE',  ( -30.72370968135370006, -6.660959539311599897, -2.999707106781269950 ) ) ;
#18146=VERTEX_POINT ( 'NONE', #1748 ) ;
#18168=CYLINDRICAL_SURFACE ( 'NONE', #11129, 0.0009999999998218898900 ) ;
#18317=VECTOR ( 'NONE', #9020, 999.9999999999998863 ) ;
#18327=ORIENTED_EDGE ( 'NONE', *, *, #3485, .T. ) ;
#18384=ORIENTED_EDGE ( 'NONE', *, *, #17625, .T. ) ;
#18437=EDGE_CURVE ( 'NONE', #17265, #20139, #14213, .T. ) ;
#18442=ORIENTED_EDGE ( 'NONE', *, *, #6640, .T. ) ;
#18477=DIRECTION ( 'NONE',  ( 1.187319687680494078E-16, 2.805478249478345354E-20, 1.000000000000000000 ) ) ;
#18479=ORIENTED_EDGE ( 'NONE', *, *, #3485, .F. ) ;
#18480=ORIENTED_EDGE ( 'NONE', *, *, #7826, .T. ) ;
#18496=EDGE_CURVE ( 'NONE', #13515, #20139, #1371, .T. ) ;
#18539=DIRECTION ( 'NONE',  ( -0.005235963827121941846, 0.9999862922474492821, 0.000000000000000000 ) ) ;
#18540=VECTOR ( 'NONE', #3240, 999.9999999999998863 ) ;
#18541=DIRECTION ( 'NONE',  ( 3.330999558972852107E-36, 2.805478249484880275E-20, 1.000000000000000000 ) ) ;
#18553=CARTESIAN_POINT ( 'NONE',  ( 3.499952022866072543, 0.01832587339492648335, -8.931114213653268455E-14 ) ) ;
#18667=CARTESIAN_POINT ( 'NONE',  ( -22.99995202268987171, -0.1204285676208968203, -8.616475246431379602E-14 ) ) ;
#18720=AXIS2_PLACEMENT_3D ( 'NONE', #19597, #16142, #7025 ) ;
#18735=ORIENTED_EDGE ( 'NONE', *, *, #1282, .F. ) ;
#18737=VERTEX_POINT ( 'NONE', #11140 ) ;
#18758=FACE_OUTER_BOUND ( 'NONE', #21278, .T. ) ;
#18763=CIRCLE ( 'NONE', #17617, 3.499999999999998224 ) ;
#18808=ORIENTED_EDGE ( 'NONE', *, *, #17625, .F. ) ;
#18818=ORIENTED_EDGE ( 'NONE', *, *, #16814, .F. ) ;
#18857=LINE ( 'NONE', #7684, #4883 ) ;
#18890=CARTESIAN_POINT ( 'NONE',  ( -28.52462712253550237, 6.350733138482030249, -0.7325259402521649976 ) ) ;
#18900=LINE ( 'NONE', #9874, #23210 ) ;
#18930=DIRECTION ( 'NONE',  ( -1.187319687680499994E-16, -2.805478249478695031E-20, -1.000000000000000000 ) ) ;
#18943=VERTEX_POINT ( 'NONE', #5046 ) ;
#18982=VECTOR ( 'NONE', #22848, 1000.000000000000000 ) ;
#18990=ORIENTED_EDGE ( 'NONE', *, *, #17655, .F. ) ;
#19002=ORIENTED_EDGE ( 'NONE', *, *, #10678, .F. ) ;
#19041=DIRECTION ( 'NONE',  ( -1.187319687680494078E-16, -2.805478249478340539E-20, -1.000000000000000000 ) ) ;
#19098=CARTESIAN_POINT ( 'NONE',  ( -16.00004797695772751, -0.08377682083104273647, -2.500000000000090594 ) ) ;
#19124=ORIENTED_EDGE ( 'NONE', *, *, #16627, .T. ) ;
#19130=CYLINDRICAL_SURFACE ( 'NONE', #3718, 3.499999999999998224 ) ;
#19181=DIRECTION ( 'NONE',  ( -1.187319687680494078E-16, -2.805478249478340539E-20, -1.000000000000000000 ) ) ;
#19189=CARTESIAN_POINT ( 'NONE',  ( 1.836479826415680084E-19, -7.772252928343919938E-16, -8.889558542813568797E-14 ) ) ;
#19211=ORIENTED_EDGE ( 'NONE', *, *, #1779, .T. ) ;
#19213=CARTESIAN_POINT ( 'NONE',  ( -26.75617730459320143, 6.359992804688680224, -2.500000000000090150 ) ) ;
#19242=EDGE_CURVE ( 'NONE', #3314, #18737, #10988, .T. ) ;
#19301=VERTEX_POINT ( 'NONE', #23312 ) ;
#19302=DIRECTION ( 'NONE',  ( -1.187319687680494078E-16, -2.805478249478340539E-20, -1.000000000000000000 ) ) ;
#19373=DIRECTION ( 'NONE',  ( -1.187319687680499994E-16, -2.805478249478705262E-20, -1.000000000000000000 ) ) ;
#19408=LINE ( 'NONE', #23186, #12639 ) ;
#19435=PLANE ( 'NONE',  #21639 ) ;
#19444=EDGE_LOOP ( 'NONE', ( #15020, #11781 ) ) ;
#19539=CARTESIAN_POINT ( 'NONE',  ( -28.45655959278310121, -6.649088660734180145, -0.7325259402522680263 ) ) ;
#19555=CARTESIAN_POINT ( 'NONE',  ( -11.34268231757140022, -0.05939068843019929683, -8.754884475926699325E-14 ) ) ;
#19563=ORIENTED_EDGE ( 'NONE', *, *, #10678, .T. ) ;
#19574=ADVANCED_FACE ( 'NONE', ( #20923 ), #15461, .F. ) ;
#19597=CARTESIAN_POINT ( 'NONE',  ( -69.90454993788389970, 6.134066389438220135, 0.7502499999999270308 ) ) ;
#19759=DIRECTION ( 'NONE',  ( 1.329038238457898285E-16, -2.538252868458137019E-14, 1.000000000000000000 ) ) ;
#19855=EDGE_LOOP ( 'NONE', ( #11616, #18808, #4412, #3715 ) ) ;
#19934=ORIENTED_EDGE ( 'NONE', *, *, #19242, .T. ) ;
#19942=VECTOR ( 'NONE', #2117, 999.9999999999998863 ) ;
#19956=CARTESIAN_POINT ( 'NONE',  ( -19.49999999982379961, -0.1021026942259700004, -2.500000000000090150 ) ) ;
#20058=ORIENTED_EDGE ( 'NONE', *, *, #23202, .T. ) ;
#20079=DIRECTION ( 'NONE',  ( 0.005235963827121942714, -0.9999862922474493931, -2.738609489598291197E-14 ) ) ;
#20111=LINE ( 'NONE', #14999, #18114 ) ;
#20139=VERTEX_POINT ( 'NONE', #14568 ) ;
#20352=CARTESIAN_POINT ( 'NONE',  ( -26.68810977484059777, -6.639828994528159889, -2.500000000000090150 ) ) ;
#20361=DIRECTION ( 'NONE',  ( 3.330999558967088958E-36, 2.805478249480050404E-20, 1.000000000000000000 ) ) ;
#20381=CYLINDRICAL_SURFACE ( 'NONE', #4094, 3.499999999999998668 ) ;
#20385=VERTEX_POINT ( 'NONE', #753 ) ;
#20475=DIRECTION ( 'NONE',  ( 0.9999862922474493931, 0.005235963827101436548, -1.187304881134279227E-16 ) ) ;
#20498=ORIENTED_EDGE ( 'NONE', *, *, #17781, .T. ) ;
#20541=FACE_OUTER_BOUND ( 'NONE', #16424, .T. ) ;
#20558=EDGE_CURVE ( 'NONE', #903, #13085, #6834, .T. ) ;
#20675=CARTESIAN_POINT ( 'NONE',  ( -30.79248430819439974, 6.338858557519089665, -2.999000000000079602 ) ) ;
#20711=FACE_OUTER_BOUND ( 'NONE', #19855, .T. ) ;
#20814=AXIS2_PLACEMENT_3D ( 'NONE', #20675, #17463, #951 ) ;
#20871=EDGE_CURVE ( 'NONE', #13431, #15347, #971, .T. ) ;
#20923=FACE_OUTER_BOUND ( 'NONE', #3110, .T. ) ;
#21073=DIRECTION ( 'NONE',  ( -0.005235963827101446089, 0.9999862922474493931, 5.936218956632777928E-19 ) ) ;
#21092=DIRECTION ( 'NONE',  ( 3.330999558967088958E-36, 2.805478249480050404E-20, 1.000000000000000000 ) ) ;
#21134=CARTESIAN_POINT ( 'NONE',  ( -30.72441677844210162, -6.660963241697119841, -2.999000000000090260 ) ) ;
#21176=EDGE_CURVE ( 'NONE', #9333, #15872, #21965, .T. ) ;
#21205=DIRECTION ( 'NONE',  ( 1.000000000000000000, -1.187319687680499994E-16, 0.000000000000000000 ) ) ;
#21247=CIRCLE ( 'NONE', #6858, 0.0009999999999225038516 ) ;
#21255=EDGE_LOOP ( 'NONE', ( #6712, #1401, #16580, #5528 ) ) ;
#21277=AXIS2_PLACEMENT_3D ( 'NONE', #16832, #6265, #17192 ) ;
#21278=EDGE_LOOP ( 'NONE', ( #11669, #19563, #8886, #6177, #10788, #11854, #6761, #5834, #20058, #14623, #697, #5646 ) ) ;
#21371=ORIENTED_EDGE ( 'NONE', *, *, #6971, .F. ) ;
#21398=VERTEX_POINT ( 'NONE', #5945 ) ;
#21408=CARTESIAN_POINT ( 'NONE',  ( -28.52462712253550237, 6.350733138482030249, -0.7325259402521629992 ) ) ;
#21409=ADVANCED_FACE ( 'NONE', ( #4048 ), #9519, .T. ) ;
#21440=VERTEX_POINT ( 'NONE', #18553 ) ;
#21482=VECTOR ( 'NONE', #10543, 1000.000000000000114 ) ;
#21493=CARTESIAN_POINT ( 'NONE',  ( 1.132413798561739802E-13, -1.842903579429180027E-16, -8.889558542813568797E-14 ) ) ;
#21564=CLOSED_SHELL ( 'NONE', ( #949, #11741, #3540, #7778, #16601, #21409, #16176, #12153, #5613, #3054, #7833, #21703, #19574, #12023, #17477, #3654, #2507, #23329 ) ) ;
#21569=SHAPE_REPRESENTATION ( '1602p_c_07', ( #12739 ), #21969 ) ;
#21639=AXIS2_PLACEMENT_3D ( 'NONE', #19555, #21092, #21205 ) ;
#21689=ORIENTED_EDGE ( 'NONE', *, *, #6640, .F. ) ;
#21703=ADVANCED_FACE ( 'NONE', ( #552 ), #11859, .T. ) ;
#21816=EDGE_LOOP ( 'NONE', ( #18479, #4071, #910, #14671 ) ) ;
#21866=VERTEX_POINT ( 'NONE', #12099 ) ;
#21912=ORIENTED_EDGE ( 'NONE', *, *, #23415, .F. ) ;
#21929=EDGE_CURVE ( 'NONE', #22384, #22900, #6852, .T. ) ;
#21959=ORIENTED_EDGE ( 'NONE', *, *, #13106, .F. ) ;
#21965=LINE ( 'NONE', #7276, #22223 ) ;
#21966=EDGE_CURVE ( 'NONE', #17265, #13085, #13253, .T. ) ;
#21969=( GEOMETRIC_REPRESENTATION_CONTEXT ( 3 ) GLOBAL_UNCERTAINTY_ASSIGNED_CONTEXT ( ( #6266 ) ) GLOBAL_UNIT_ASSIGNED_CONTEXT ( ( #13093, #2262, #9882 ) ) REPRESENTATION_CONTEXT ( 'NONE', 'WORKASPACE' ) );
#21978=DIRECTION ( 'NONE',  ( 4.906471675765221317E-19, -0.9999862926232440108, -0.005235892055781489474 ) ) ;
#21982=CYLINDRICAL_SURFACE ( 'NONE', #12994, 0.0009999999999615351298 ) ;
#21983=VERTEX_POINT ( 'NONE', #2203 ) ;
#22008=PRODUCT_DEFINITION_FORMATION_WITH_SPECIFIED_SOURCE ( 'ANY', '', #12523, .NOT_KNOWN. ) ;
#22032=DIRECTION ( 'NONE',  ( 0.9999862922474493931, 0.005235963827116132258, -1.187304881134280213E-16 ) ) ;
#22075=CARTESIAN_POINT ( 'NONE',  ( -30.79177721110609767, 6.338862259904598950, -2.999707106781159816 ) ) ;
#22076=PLANE ( 'NONE',  #12266 ) ;
#22080=CIRCLE ( 'NONE', #15260, 3.499999999999998668 ) ;
#22136=CARTESIAN_POINT ( 'NONE',  ( -11.34268231757140022, -0.05939068843019929683, -2.500000000000090150 ) ) ;
#22195=DIRECTION ( 'NONE',  ( 1.000000000000000000, -1.187319687680510101E-16, 0.000000000000000000 ) ) ;
#22223=VECTOR ( 'NONE', #16511, 1000.000000000000114 ) ;
#22249=ORIENTED_EDGE ( 'NONE', *, *, #1355, .F. ) ;
#22272=CARTESIAN_POINT ( 'NONE',  ( -28.95596696049959817, -6.651703575491109355, -4.767474059747899950 ) ) ;
#22303=VERTEX_POINT ( 'NONE', #14415 ) ;
#22314=ORIENTED_EDGE ( 'NONE', *, *, #7826, .F. ) ;
#22370=DIRECTION ( 'NONE',  ( -0.7070970883417637687, -0.003702385528197202434, 0.7071067811865479058 ) ) ;
#22377=AXIS2_PLACEMENT_3D ( 'NONE', #12738, #20079, #4051 ) ;
#22384=VERTEX_POINT ( 'NONE', #10529 ) ;
#22469=ORIENTED_EDGE ( 'NONE', *, *, #12962, .F. ) ;
#22498=AXIS2_PLACEMENT_3D ( 'NONE', #21493, #19373, #12147 ) ;
#22540=ORIENTED_EDGE ( 'NONE', *, *, #21966, .F. ) ;
#22595=DIRECTION ( 'NONE',  ( 1.000000000000000000, -1.187319687680499994E-16, 0.000000000000000000 ) ) ;
#22601=EDGE_CURVE ( 'NONE', #22900, #9333, #1029, .T. ) ;
#22618=DIRECTION ( 'NONE',  ( -0.7070970883417647679, -0.003702385528188428636, -0.7071067811865467956 ) ) ;
#22626=CARTESIAN_POINT ( 'NONE',  ( -26.72214353971689960, -0.1399180949199879953, -2.500999999999910184 ) ) ;
#22657=ORIENTED_EDGE ( 'NONE', *, *, #192, .T. ) ;
#22682=ORIENTED_EDGE ( 'NONE', *, *, #2258, .F. ) ;
#22692=ORIENTED_EDGE ( 'NONE', *, *, #2108, .T. ) ;
#22701=CARTESIAN_POINT ( 'NONE',  ( 1.132413798561739802E-13, -1.842903579429180027E-16, -8.889558542813568797E-14 ) ) ;
#22720=VERTEX_POINT ( 'NONE', #12168 ) ;
#22743=DESIGN_CONTEXT ( 'detailed design', #2331, 'design' ) ;
#22813=ORIENTED_EDGE ( 'NONE', *, *, #6201, .F. ) ;
#22848=DIRECTION ( 'NONE',  ( -1.187319687680499994E-16, -2.805478249478640262E-20, -1.000000000000000000 ) ) ;
#22900=VERTEX_POINT ( 'NONE', #12929 ) ;
#23002=VECTOR ( 'NONE', #22032, 1000.000000000000000 ) ;
#23128=ORIENTED_EDGE ( 'NONE', *, *, #16504, .T. ) ;
#23186=CARTESIAN_POINT ( 'NONE',  ( -16.00004797695773107, -0.08377682083104275035, -8.699586588110780178E-14 ) ) ;
#23193=EDGE_CURVE ( 'NONE', #18943, #18146, #13758, .T. ) ;
#23202=EDGE_CURVE ( 'NONE', #15872, #13648, #3613, .T. ) ;
#23210=VECTOR ( 'NONE', #592, 1000.000000000000114 ) ;
#23219=CIRCLE ( 'NONE', #5784, 3.499999999999998224 ) ;
#23312=CARTESIAN_POINT ( 'NONE',  ( -22.99995202268987171, -0.1204285676208968203, -2.500000000000089706 ) ) ;
#23329=ADVANCED_FACE ( 'NONE', ( #7341 ), #9234, .T. ) ;
#23332=EDGE_LOOP ( 'NONE', ( #20498, #22657 ) ) ;
#23402=VECTOR ( 'NONE', #4542, 999.9999999999998863 ) ;
#23415=EDGE_CURVE ( 'NONE', #13431, #21440, #16513, .T. ) ;
#23441=LINE ( 'NONE', #3507, #10797 ) ;
#23463=DIRECTION ( 'NONE',  ( -1.187319687680494078E-16, -2.805478249478345354E-20, -1.000000000000000000 ) ) ;
#23550=COLOUR_RGB('Black', 0.08235294, 0.09019608, 0.10196078);
#23551=FILL_AREA_STYLE_COLOUR('',#23550);
#23552=FILL_AREA_STYLE('',(#23551));
#23553=SURFACE_STYLE_FILL_AREA(#23552);
#23554=SURFACE_SIDE_STYLE('',(#23553));
#23555=SURFACE_STYLE_USAGE(.BOTH.,#23554);
#23556=PRESENTATION_STYLE_ASSIGNMENT((#23555));
#23567=STYLED_ITEM('',(#23556),#9741);
#23568=MECHANICAL_DESIGN_GEOMETRIC_PRESENTATION_REPRESENTATION('',(#23567),#21969);
ENDSEC;
END-ISO-10303-21;
